ISO-10303-21;
HEADER;
FILE_DESCRIPTION (('STEP AP214'),
    '1' );
FILE_NAME ('Joint Plane.step',
    '2026-10-28T16:39:03',
    ( '' ),
    ( '' ),
    'SwSTEP 2.0',
    'SolidWorks 2024',
    '' );
FILE_SCHEMA (( 'AUTOMOTIVE_DESIGN' ));
ENDSEC;

DATA;
#19=LINE ( 'NONE', #1821, #4426 ) ;
#23=CARTESIAN_POINT ( 'NONE',  ( -74.28095588234631919, 12.70544120911856112, 12.50000000000000000 ) ) ;
#39=DIRECTION ( 'NONE',  ( 1.000000000000000000, 0.000000000000000000, 0.000000000000000000 ) ) ;
#47=CARTESIAN_POINT ( 'NONE',  ( -24.28095581706361727, -30.59582894744887582, 0.000000000000000000 ) ) ;
#52=VERTEX_POINT ( 'NONE', #7725 ) ;
#56=CARTESIAN_POINT ( 'NONE',  ( 0.7190441502950353225, 87.70544117646394966, 0.000000000000000000 ) ) ;
#59=ORIENTED_EDGE ( 'NONE', *, *, #2376, .F. ) ;
#83=CARTESIAN_POINT ( 'NONE',  ( 25.71904415029483459, 19.40417101989674009, 12.50000000000000000 ) ) ;
#88=CARTESIAN_POINT ( 'NONE',  ( 47.36967921662626679, 6.904171036223937463, 0.000000000000000000 ) ) ;
#108=LINE ( 'NONE', #6772, #1142 ) ;
#112=VECTOR ( 'NONE', #5302, 1000.000000000000000 ) ;
#130=CARTESIAN_POINT ( 'NONE',  ( 72.36967921662629522, 50.20544122544588816, 12.50000000000000000 ) ) ;
#134=EDGE_CURVE ( 'NONE', #6179, #1386, #5939, .T. ) ;
#141=DIRECTION ( 'NONE',  ( -0.000000000000000000, 0.000000000000000000, 1.000000000000000000 ) ) ;
#145=DIRECTION ( 'NONE',  ( -0.000000000000000000, -0.000000000000000000, -1.000000000000000000 ) ) ;
#146=VECTOR ( 'NONE', #1608, 1000.000000000000000 ) ;
#165=DIRECTION ( 'NONE',  ( 0.000000000000000000, 1.000000000000000000, -0.000000000000000000 ) ) ;
#185=VECTOR ( 'NONE', #4899, 1000.000000000000000 ) ;
#199=CARTESIAN_POINT ( 'NONE',  ( 13.21904415029483459, 19.40417101989674009, 0.000000000000000000 ) ) ;
#201=ORIENTED_EDGE ( 'NONE', *, *, #2548, .F. ) ;
#202=CYLINDRICAL_SURFACE ( 'NONE', #7486, 24.99999996734561236 ) ;
#211=ORIENTED_EDGE ( 'NONE', *, *, #2498, .T. ) ;
#212=CIRCLE ( 'NONE', #5597, 24.99999998367932719 ) ;
#217=CARTESIAN_POINT ( 'NONE',  ( -36.78095584970496645, -62.29455879088143888, 12.50000000000000000 ) ) ;
#227=DIRECTION ( 'NONE',  ( 1.000000000000000000, 0.000000000000000000, 0.000000000000000000 ) ) ;
#241=AXIS2_PLACEMENT_3D ( 'NONE', #5077, #7569, #7530 ) ;
#244=APPLICATION_CONTEXT ( 'automotive_design' ) ;
#251=EDGE_CURVE ( 'NONE', #1936, #5801, #2874, .T. ) ;
#255=DIRECTION ( 'NONE',  ( 0.000000000000000000, 1.000000000000000000, 0.000000000000000000 ) ) ;
#273=EDGE_CURVE ( 'NONE', #7797, #819, #1208, .T. ) ;
#276=EDGE_CURVE ( 'NONE', #5902, #5001, #2575, .T. ) ;
#284=DIRECTION ( 'NONE',  ( 0.7070068166729618353, 0.7072067315700302226, 0.000000000000000000 ) ) ;
#288=CYLINDRICAL_SURFACE ( 'NONE', #5824, 12.50000000000000000 ) ;
#306=AXIS2_PLACEMENT_3D ( 'NONE', #1196, #5333, #4802 ) ;
#308=VERTEX_POINT ( 'NONE', #56 ) ;
#310=ORIENTED_EDGE ( 'NONE', *, *, #7912, .F. ) ;
#326=DIRECTION ( 'NONE',  ( -0.000000000000000000, -0.000000000000000000, -1.000000000000000000 ) ) ;
#330=ADVANCED_FACE ( 'NONE', ( #6803 ), #6719, .T. ) ;
#334=VERTEX_POINT ( 'NONE', #6163 ) ;
#339=EDGE_LOOP ( 'NONE', ( #7598, #1721, #7213, #3654 ) ) ;
#344=CARTESIAN_POINT ( 'NONE',  ( 0.7190441502950423169, -5.595828947448873159, 12.50000000000000000 ) ) ;
#365=VECTOR ( 'NONE', #813, 1000.000000000000000 ) ;
#383=CARTESIAN_POINT ( 'NONE',  ( 0.000000000000000000, 0.000000000000000000, 12.50000000000000000 ) ) ;
#390=ORIENTED_EDGE ( 'NONE', *, *, #7784, .F. ) ;
#391=DIRECTION ( 'NONE',  ( -1.000000000000000000, 0.000000000000000000, 0.000000000000000000 ) ) ;
#404=LINE ( 'NONE', #1042, #2411 ) ;
#412=CARTESIAN_POINT ( 'NONE',  ( 38.21904415029484170, 19.40417101989674009, 0.000000000000000000 ) ) ;
#414=EDGE_CURVE ( 'NONE', #2350, #2221, #5040, .T. ) ;
#417=CARTESIAN_POINT ( 'NONE',  ( 13.21904415029483459, 19.40417101989674009, 12.50000000000000000 ) ) ;
#420=EDGE_CURVE ( 'NONE', #3389, #4483, #5139, .T. ) ;
#434=ORIENTED_EDGE ( 'NONE', *, *, #5862, .T. ) ;
#445=LINE ( 'NONE', #2814, #3060 ) ;
#448=AXIS2_PLACEMENT_3D ( 'NONE', #7739, #4869, #4683 ) ;
#457=CARTESIAN_POINT ( 'NONE',  ( 25.71904415029483459, 19.40417101989674009, 12.50000000000000000 ) ) ;
#464=ORIENTED_EDGE ( 'NONE', *, *, #7246, .F. ) ;
#475=( NAMED_UNIT ( * ) PLANE_ANGLE_UNIT ( ) SI_UNIT ( $, .RADIAN. ) );
#479=CARTESIAN_POINT ( 'NONE',  ( -24.28095581706361372, 2.657566677470048251E-15, 0.000000000000000000 ) ) ;
#520=EDGE_LOOP ( 'NONE', ( #5499, #7180, #5921, #6159 ) ) ;
#522=ORIENTED_EDGE ( 'NONE', *, *, #7865, .F. ) ;
#527=CARTESIAN_POINT ( 'NONE',  ( 0.7190441502950353225, 87.70544117646394966, 12.50000000000000000 ) ) ;
#528=ADVANCED_FACE ( 'NONE', ( #7165 ), #5426, .F. ) ;
#540=CARTESIAN_POINT ( 'NONE',  ( 25.71904415029483459, -5.595828947448873159, 12.50000000000000000 ) ) ;
#548=EDGE_LOOP ( 'NONE', ( #3367, #4727, #4586, #2245 ) ) ;
#565=ORIENTED_EDGE ( 'NONE', *, *, #7553, .F. ) ;
#575=AXIS2_PLACEMENT_3D ( 'NONE', #4907, #4309, #1270 ) ;
#601=CARTESIAN_POINT ( 'NONE',  ( 63.21904415029505486, 62.70544120911855401, 0.000000000000000000 ) ) ;
#608=ORIENTED_EDGE ( 'NONE', *, *, #3986, .F. ) ;
#629=ORIENTED_EDGE ( 'NONE', *, *, #810, .F. ) ;
#638=UNCERTAINTY_MEASURE_WITH_UNIT (LENGTH_MEASURE( 1.000000000000000082E-05 ), #3084, 'distance_accuracy_value', 'NONE');
#652=CARTESIAN_POINT ( 'NONE',  ( 0.7190441502950353225, 62.70544120911855401, 0.000000000000000000 ) ) ;
#669=EDGE_CURVE ( 'NONE', #7782, #6179, #2463, .T. ) ;
#671=DIRECTION ( 'NONE',  ( -0.000000000000000000, -0.000000000000000000, -1.000000000000000000 ) ) ;
#674=ORIENTED_EDGE ( 'NONE', *, *, #4625, .T. ) ;
#676=ADVANCED_BREP_SHAPE_REPRESENTATION ( '', ( #4034, #5785 ), #3097 ) ;
#678=EDGE_LOOP ( 'NONE', ( #1523, #3489, #674, #1591 ) ) ;
#701=DIRECTION ( 'NONE',  ( -0.000000000000000000, -0.000000000000000000, -1.000000000000000000 ) ) ;
#705=DIRECTION ( 'NONE',  ( -1.000000000000000000, 0.000000000000000000, 0.000000000000000000 ) ) ;
#713=ORIENTED_EDGE ( 'NONE', *, *, #134, .T. ) ;
#730=CIRCLE ( 'NONE', #861, 25.00000003264134918 ) ;
#744=CARTESIAN_POINT ( 'NONE',  ( 72.36967921662629522, 50.20544122544588816, 0.000000000000000000 ) ) ;
#754=CIRCLE ( 'NONE', #5883, 12.50000000000000355 ) ;
#781=VERTEX_POINT ( 'NONE', #3716 ) ;
#784=VERTEX_POINT ( 'NONE', #3111 ) ;
#795=ORIENTED_EDGE ( 'NONE', *, *, #3102, .T. ) ;
#807=DIRECTION ( 'NONE',  ( 0.000000000000000000, -0.000000000000000000, 1.000000000000000000 ) ) ;
#810=EDGE_CURVE ( 'NONE', #52, #5747, #3752, .T. ) ;
#813=DIRECTION ( 'NONE',  ( -0.000000000000000000, -0.000000000000000000, -1.000000000000000000 ) ) ;
#815=ORIENTED_EDGE ( 'NONE', *, *, #6606, .F. ) ;
#818=DIRECTION ( 'NONE',  ( -0.000000000000000000, -0.000000000000000000, -1.000000000000000000 ) ) ;
#819=VERTEX_POINT ( 'NONE', #1371 ) ;
#838=VECTOR ( 'NONE', #145, 1000.000000000000000 ) ;
#849=CARTESIAN_POINT ( 'NONE',  ( -74.28095588234631919, 0.000000000000000000, 12.50000000000000000 ) ) ;
#852=VECTOR ( 'NONE', #1540, 1000.000000000000000 ) ;
#855=EDGE_CURVE ( 'NONE', #7362, #1918, #6307, .T. ) ;
#856=CARTESIAN_POINT ( 'NONE',  ( -36.78095584970496645, 12.70544120911856290, 12.50000000000000000 ) ) ;
#861=AXIS2_PLACEMENT_3D ( 'NONE', #1725, #3660, #4213 ) ;
#865=ADVANCED_FACE ( 'NONE', ( #7030 ), #288, .F. ) ;
#869=VERTEX_POINT ( 'NONE', #4497 ) ;
#879=ORIENTED_EDGE ( 'NONE', *, *, #2053, .F. ) ;
#882=DIRECTION ( 'NONE',  ( -0.000000000000000000, 0.000000000000000000, 1.000000000000000000 ) ) ;
#893=CARTESIAN_POINT ( 'NONE',  ( -11.78095584970496290, 62.70544120911855401, 12.50000000000000000 ) ) ;
#903=ADVANCED_FACE ( 'NONE', ( #5751 ), #3376, .T. ) ;
#908=CIRCLE ( 'NONE', #4747, 24.99999996734560881 ) ;
#928=EDGE_CURVE ( 'NONE', #5929, #1635, #5169, .T. ) ;
#962=DIRECTION ( 'NONE',  ( 1.000000000000000000, 0.000000000000000000, 0.000000000000000000 ) ) ;
#964=CIRCLE ( 'NONE', #1601, 12.50000000000000355 ) ;
#966=CARTESIAN_POINT ( 'NONE',  ( -49.28095584970496645, 12.70544120911856112, 0.000000000000000000 ) ) ;
#972=DIRECTION ( 'NONE',  ( -0.000000000000000000, 0.000000000000000000, 1.000000000000000000 ) ) ;
#999=EDGE_LOOP ( 'NONE', ( #5153, #5490, #4822, #6178 ) ) ;
#1006=ORIENTED_EDGE ( 'NONE', *, *, #6028, .T. ) ;
#1022=EDGE_LOOP ( 'NONE', ( #5127, #3440, #6797, #1983 ) ) ;
#1025=CARTESIAN_POINT ( 'NONE',  ( -49.28095584970496645, -62.29455879088143888, 12.50000000000000000 ) ) ;
#1042=CARTESIAN_POINT ( 'NONE',  ( -24.28095581706362083, -62.29455879088143888, 12.50000000000000000 ) ) ;
#1047=FACE_BOUND ( 'NONE', #5656, .T. ) ;
#1048=DIRECTION ( 'NONE',  ( -0.000000000000000000, -0.000000000000000000, -1.000000000000000000 ) ) ;
#1053=DIRECTION ( 'NONE',  ( -0.000000000000000000, 0.000000000000000000, 1.000000000000000000 ) ) ;
#1060=ORIENTED_EDGE ( 'NONE', *, *, #5526, .T. ) ;
#1066=EDGE_CURVE ( 'NONE', #7250, #1386, #7194, .T. ) ;
#1070=LINE ( 'NONE', #479, #7244 ) ;
#1087=AXIS2_PLACEMENT_3D ( 'NONE', #7280, #1854, #2957 ) ;
#1091=CARTESIAN_POINT ( 'NONE',  ( 63.21904415029505486, 62.70544120911855401, 12.50000000000000000 ) ) ;
#1124=AXIS2_PLACEMENT_3D ( 'NONE', #3011, #3737, #5570 ) ;
#1125=VECTOR ( 'NONE', #4265, 1000.000000000000114 ) ;
#1126=DIRECTION ( 'NONE',  ( -1.000000000000000000, 0.000000000000000000, 0.000000000000000000 ) ) ;
#1141=VERTEX_POINT ( 'NONE', #5462 ) ;
#1142=VECTOR ( 'NONE', #671, 1000.000000000000000 ) ;
#1163=EDGE_CURVE ( 'NONE', #1336, #1401, #3620, .T. ) ;
#1169=DIRECTION ( 'NONE',  ( -0.000000000000000000, -0.000000000000000000, -1.000000000000000000 ) ) ;
#1196=CARTESIAN_POINT ( 'NONE',  ( 50.71904415029504065, 62.70544120911855401, 12.50000000000000000 ) ) ;
#1203=DIRECTION ( 'NONE',  ( 0.000000000000000000, -1.000000000000000000, 0.000000000000000000 ) ) ;
#1208=CIRCLE ( 'NONE', #6844, 12.50000000000000355 ) ;
#1220=VECTOR ( 'NONE', #2563, 1000.000000000000000 ) ;
#1228=LINE ( 'NONE', #5600, #1125 ) ;
#1236=ORIENTED_EDGE ( 'NONE', *, *, #7150, .T. ) ;
#1239=EDGE_LOOP ( 'NONE', ( #7845, #1236, #3933, #3292 ) ) ;
#1261=VECTOR ( 'NONE', #1281, 1000.000000000000000 ) ;
#1270=DIRECTION ( 'NONE',  ( -0.7070068166729618353, -0.7072067315700302226, 0.000000000000000000 ) ) ;
#1272=ORIENTED_EDGE ( 'NONE', *, *, #6816, .F. ) ;
#1281=DIRECTION ( 'NONE',  ( -0.000000000000000000, -0.000000000000000000, -1.000000000000000000 ) ) ;
#1295=DIRECTION ( 'NONE',  ( 1.000000000000000000, 0.000000000000000000, 0.000000000000000000 ) ) ;
#1303=EDGE_CURVE ( 'NONE', #1635, #1401, #4900, .T. ) ;
#1321=LINE ( 'NONE', #7427, #6508 ) ;
#1333=CARTESIAN_POINT ( 'NONE',  ( 0.7190441502950423169, -5.595828947448873159, 12.50000000000000000 ) ) ;
#1336=VERTEX_POINT ( 'NONE', #6298 ) ;
#1349=EDGE_CURVE ( 'NONE', #781, #3736, #5424, .T. ) ;
#1353=ORIENTED_EDGE ( 'NONE', *, *, #7079, .T. ) ;
#1368=VECTOR ( 'NONE', #6947, 1000.000000000000000 ) ;
#1371=CARTESIAN_POINT ( 'NONE',  ( -36.78095584970496645, 12.70544120911856290, 12.50000000000000000 ) ) ;
#1378=CIRCLE ( 'NONE', #1786, 24.99999996734539920 ) ;
#1384=CARTESIAN_POINT ( 'NONE',  ( 0.7190441502950353225, 62.70544120911855401, 12.50000000000000000 ) ) ;
#1386=VERTEX_POINT ( 'NONE', #199 ) ;
#1388=ORIENTED_EDGE ( 'NONE', *, *, #7148, .F. ) ;
#1401=VERTEX_POINT ( 'NONE', #2166 ) ;
#1403=ADVANCED_FACE ( 'NONE', ( #2855 ), #4310, .F. ) ;
#1415=CARTESIAN_POINT ( 'NONE',  ( 13.21904415029503355, 62.70544120911855401, 12.50000000000000000 ) ) ;
#1424=DIRECTION ( 'NONE',  ( 1.000000000000000000, 0.000000000000000000, 0.000000000000000000 ) ) ;
#1445=CARTESIAN_POINT ( 'NONE',  ( 0.000000000000000000, 87.70544117646394966, 12.50000000000000000 ) ) ;
#1452=AXIS2_PLACEMENT_3D ( 'NONE', #5182, #2789, #7518 ) ;
#1455=ORIENTED_EDGE ( 'NONE', *, *, #7150, .F. ) ;
#1474=CIRCLE ( 'NONE', #4544, 24.99999996734539920 ) ;
#1476=ORIENTED_EDGE ( 'NONE', *, *, #4050, .F. ) ;
#1483=AXIS2_PLACEMENT_3D ( 'NONE', #3399, #3956, #5924 ) ;
#1502=DIRECTION ( 'NONE',  ( -0.000000000000000000, 0.000000000000000000, 1.000000000000000000 ) ) ;
#1523=ORIENTED_EDGE ( 'NONE', *, *, #7264, .F. ) ;
#1525=CARTESIAN_POINT ( 'NONE',  ( 50.71904415029504065, 62.70544120911855401, 0.000000000000000000 ) ) ;
#1526=PLANE ( 'NONE',  #4963 ) ;
#1534=CARTESIAN_POINT ( 'NONE',  ( 0.000000000000000000, -5.595828947448873159, 12.50000000000000000 ) ) ;
#1540=DIRECTION ( 'NONE',  ( -0.5000000000000004441, -0.8660254037844383745, 0.000000000000000000 ) ) ;
#1550=ADVANCED_FACE ( 'NONE', ( #2708 ), #6924, .T. ) ;
#1553=EDGE_CURVE ( 'NONE', #819, #7797, #4539, .T. ) ;
#1561=DIRECTION ( 'NONE',  ( -0.000000000000000000, 0.000000000000000000, 1.000000000000000000 ) ) ;
#1572=ORIENTED_EDGE ( 'NONE', *, *, #2376, .T. ) ;
#1580=CARTESIAN_POINT ( 'NONE',  ( 25.71904415029483459, 19.40417101989674009, 0.000000000000000000 ) ) ;
#1591=ORIENTED_EDGE ( 'NONE', *, *, #1163, .T. ) ;
#1594=EDGE_LOOP ( 'NONE', ( #7601, #815, #608, #1006 ) ) ;
#1601=AXIS2_PLACEMENT_3D ( 'NONE', #2217, #972, #2132 ) ;
#1603=DIRECTION ( 'NONE',  ( -0.000000000000000000, -0.000000000000000000, -1.000000000000000000 ) ) ;
#1606=LINE ( 'NONE', #4008, #1368 ) ;
#1608=DIRECTION ( 'NONE',  ( -0.000000000000000000, -0.000000000000000000, -1.000000000000000000 ) ) ;
#1635=VERTEX_POINT ( 'NONE', #744 ) ;
#1643=CIRCLE ( 'NONE', #6129, 12.50000000000000355 ) ;
#1652=FACE_OUTER_BOUND ( 'NONE', #7190, .T. ) ;
#1658=DIRECTION ( 'NONE',  ( -0.000000000000000000, 0.000000000000000000, 1.000000000000000000 ) ) ;
#1682=DIRECTION ( 'NONE',  ( -0.000000000000000000, -0.000000000000000000, -1.000000000000000000 ) ) ;
#1684=PRODUCT_DEFINITION_FORMATION_WITH_SPECIFIED_SOURCE ( 'ANY', '', #6933, .NOT_KNOWN. ) ;
#1688=CARTESIAN_POINT ( 'NONE',  ( 0.000000000000000000, -5.595828947448873159, 12.50000000000000000 ) ) ;
#1702=ORIENTED_EDGE ( 'NONE', *, *, #5682, .F. ) ;
#1703=ORIENTED_EDGE ( 'NONE', *, *, #1553, .T. ) ;
#1709=ADVANCED_FACE ( 'NONE', ( #2100, #2790, #7077, #2871, #3477, #7597 ), #5225, .T. ) ;
#1720=ORIENTED_EDGE ( 'NONE', *, *, #7865, .T. ) ;
#1721=ORIENTED_EDGE ( 'NONE', *, *, #6028, .F. ) ;
#1725=CARTESIAN_POINT ( 'NONE',  ( -49.28095584970496645, 12.70544120911856112, 0.000000000000000000 ) ) ;
#1732=CARTESIAN_POINT ( 'NONE',  ( -0.000000000000000000, 87.70544117646394966, 0.000000000000000000 ) ) ;
#1745=ADVANCED_FACE ( 'NONE', ( #2347 ), #6560, .T. ) ;
#1786=AXIS2_PLACEMENT_3D ( 'NONE', #6056, #7304, #1800 ) ;
#1800=DIRECTION ( 'NONE',  ( 1.000000000000000000, 0.000000000000000000, 0.000000000000000000 ) ) ;
#1821=CARTESIAN_POINT ( 'NONE',  ( -36.78095584970496645, -62.29455879088143888, 12.50000000000000000 ) ) ;
#1832=CARTESIAN_POINT ( 'NONE',  ( -24.28095581706361372, 2.657566677470048251E-15, 12.50000000000000000 ) ) ;
#1839=ORIENTED_EDGE ( 'NONE', *, *, #5026, .T. ) ;
#1840=CARTESIAN_POINT ( 'NONE',  ( 13.21904415029503355, 62.70544120911855401, 12.50000000000000000 ) ) ;
#1854=DIRECTION ( 'NONE',  ( 0.8660254037844383745, -0.5000000000000004441, 0.000000000000000000 ) ) ;
#1855=CIRCLE ( 'NONE', #2503, 12.49999999999999822 ) ;
#1887=CARTESIAN_POINT ( 'NONE',  ( 38.21904415029501934, 62.70544120911855401, 12.50000000000000000 ) ) ;
#1889=VECTOR ( 'NONE', #6664, 1000.000000000000000 ) ;
#1892=CARTESIAN_POINT ( 'NONE',  ( 0.7190441666157093570, -30.59582893112819946, 12.50000000000000000 ) ) ;
#1906=CARTESIAN_POINT ( 'NONE',  ( -49.28095584970496645, 12.70544120911856112, 12.50000000000000000 ) ) ;
#1908=LINE ( 'NONE', #23, #838 ) ;
#1915=ORIENTED_EDGE ( 'NONE', *, *, #5391, .F. ) ;
#1918=VERTEX_POINT ( 'NONE', #1333 ) ;
#1935=ORIENTED_EDGE ( 'NONE', *, *, #6757, .F. ) ;
#1936=VERTEX_POINT ( 'NONE', #2616 ) ;
#1939=DIRECTION ( 'NONE',  ( 1.000000000000000000, 0.000000000000000000, 0.000000000000000000 ) ) ;
#1959=LINE ( 'NONE', #6867, #5164 ) ;
#1962=AXIS2_PLACEMENT_3D ( 'NONE', #1525, #7579, #6455 ) ;
#1983=ORIENTED_EDGE ( 'NONE', *, *, #1066, .F. ) ;
#1990=ORIENTED_EDGE ( 'NONE', *, *, #2007, .F. ) ;
#2007=EDGE_CURVE ( 'NONE', #2221, #2350, #3145, .T. ) ;
#2020=CARTESIAN_POINT ( 'NONE',  ( 50.71904415029504065, 62.70544120911855401, 0.000000000000000000 ) ) ;
#2047=LINE ( 'NONE', #3971, #4662 ) ;
#2049=FACE_OUTER_BOUND ( 'NONE', #1594, .T. ) ;
#2053=EDGE_CURVE ( 'NONE', #7250, #7782, #964, .T. ) ;
#2076=LINE ( 'NONE', #7693, #4848 ) ;
#2100=FACE_OUTER_BOUND ( 'NONE', #7135, .T. ) ;
#2121=DIRECTION ( 'NONE',  ( -1.094506615593124476E-16, -1.000000000000000000, 0.000000000000000000 ) ) ;
#2122=CYLINDRICAL_SURFACE ( 'NONE', #6718, 12.50000000000000355 ) ;
#2132=DIRECTION ( 'NONE',  ( 1.000000000000000000, 0.000000000000000000, 0.000000000000000000 ) ) ;
#2133=DIRECTION ( 'NONE',  ( 1.000000000000000000, 0.000000000000000000, 0.000000000000000000 ) ) ;
#2137=DIRECTION ( 'NONE',  ( 1.000000000000000000, 0.000000000000000000, 0.000000000000000000 ) ) ;
#2149=CARTESIAN_POINT ( 'NONE',  ( 25.71904415029483459, 19.40417101989674009, 12.50000000000000000 ) ) ;
#2156=VECTOR ( 'NONE', #3820, 1000.000000000000000 ) ;
#2160=EDGE_LOOP ( 'NONE', ( #1702, #5057 ) ) ;
#2166=CARTESIAN_POINT ( 'NONE',  ( 50.71904415029504065, 87.70544117646394966, 0.000000000000000000 ) ) ;
#2182=DIRECTION ( 'NONE',  ( -0.000000000000000000, 0.000000000000000000, 1.000000000000000000 ) ) ;
#2190=DIRECTION ( 'NONE',  ( -0.000000000000000000, -0.000000000000000000, -1.000000000000000000 ) ) ;
#2199=LINE ( 'NONE', #6097, #1261 ) ;
#2217=CARTESIAN_POINT ( 'NONE',  ( 25.71904415029483459, 19.40417101989674009, 12.50000000000000000 ) ) ;
#2221=VERTEX_POINT ( 'NONE', #1091 ) ;
#2236=CYLINDRICAL_SURFACE ( 'NONE', #3037, 12.49999999999999822 ) ;
#2241=DIRECTION ( 'NONE',  ( -0.000000000000000000, -0.000000000000000000, -1.000000000000000000 ) ) ;
#2245=ORIENTED_EDGE ( 'NONE', *, *, #134, .F. ) ;
#2257=AXIS2_PLACEMENT_3D ( 'NONE', #6008, #2241, #6050 ) ;
#2259=FACE_OUTER_BOUND ( 'NONE', #5973, .T. ) ;
#2260=CARTESIAN_POINT ( 'NONE',  ( -24.28095581706362083, -62.29455879088143888, 12.50000000000000000 ) ) ;
#2270=CARTESIAN_POINT ( 'NONE',  ( 32.53766565774834163, -18.78563002630307111, 12.50000000000000000 ) ) ;
#2273=DIRECTION ( 'NONE',  ( 1.000000000000000000, 0.000000000000000000, 0.000000000000000000 ) ) ;
#2276=ORIENTED_EDGE ( 'NONE', *, *, #6309, .T. ) ;
#2294=DIRECTION ( 'NONE',  ( -1.000000000000000000, 0.000000000000000000, 0.000000000000000000 ) ) ;
#2316=EDGE_LOOP ( 'NONE', ( #4599, #6248, #201, #5661 ) ) ;
#2347=FACE_OUTER_BOUND ( 'NONE', #520, .T. ) ;
#2350=VERTEX_POINT ( 'NONE', #1887 ) ;
#2351=DIRECTION ( 'NONE',  ( 1.000000000000000000, 0.000000000000000000, 0.000000000000000000 ) ) ;
#2360=CYLINDRICAL_SURFACE ( 'NONE', #6268, 12.49999999999999822 ) ;
#2365=FACE_OUTER_BOUND ( 'NONE', #4806, .T. ) ;
#2366=AXIS2_PLACEMENT_3D ( 'NONE', #2670, #5108, #3796 ) ;
#2376=EDGE_CURVE ( 'NONE', #5001, #5902, #7732, .T. ) ;
#2388=ADVANCED_FACE ( 'NONE', ( #3817 ), #202, .T. ) ;
#2390=ORIENTED_EDGE ( 'NONE', *, *, #7251, .F. ) ;
#2411=VECTOR ( 'NONE', #1682, 1000.000000000000000 ) ;
#2425=LINE ( 'NONE', #6791, #2156 ) ;
#2450=EDGE_LOOP ( 'NONE', ( #7615, #3602, #5433, #1388 ) ) ;
#2454=DIRECTION ( 'NONE',  ( -0.000000000000000000, 0.000000000000000000, 1.000000000000000000 ) ) ;
#2463=LINE ( 'NONE', #3788, #185 ) ;
#2466=SHAPE_REPRESENTATION_RELATIONSHIP ( 'NONE' , 'NONE' ,  #6180, #676 ) ;
#2484=EDGE_CURVE ( 'NONE', #7797, #5801, #1959, .T. ) ;
#2486=ORIENTED_EDGE ( 'NONE', *, *, #3414, .T. ) ;
#2498=EDGE_CURVE ( 'NONE', #6738, #784, #2047, .T. ) ;
#2502=CARTESIAN_POINT ( 'NONE',  ( 50.71904415029504065, 62.70544120911855401, 12.50000000000000000 ) ) ;
#2503=AXIS2_PLACEMENT_3D ( 'NONE', #6704, #3622, #4133 ) ;
#2509=DIRECTION ( 'NONE',  ( -1.000000000000000000, 0.000000000000000000, 0.000000000000000000 ) ) ;
#2532=CARTESIAN_POINT ( 'NONE',  ( 50.71904415029504065, 87.70544117646394966, 12.50000000000000000 ) ) ;
#2534=DIRECTION ( 'NONE',  ( -0.000000000000000000, -0.000000000000000000, -1.000000000000000000 ) ) ;
#2541=DIRECTION ( 'NONE',  ( -0.000000000000000000, 0.000000000000000000, 1.000000000000000000 ) ) ;
#2542=CIRCLE ( 'NONE', #241, 12.50000000000000355 ) ;
#2545=AXIS2_PLACEMENT_3D ( 'NONE', #4773, #1053, #5217 ) ;
#2548=EDGE_CURVE ( 'NONE', #5801, #1936, #5300, .T. ) ;
#2563=DIRECTION ( 'NONE',  ( -0.000000000000000000, -0.000000000000000000, -1.000000000000000000 ) ) ;
#2564=ORIENTED_EDGE ( 'NONE', *, *, #4771, .F. ) ;
#2572=ADVANCED_FACE ( 'NONE', ( #4643 ), #2122, .F. ) ;
#2575=CIRCLE ( 'NONE', #7694, 12.49999999999999822 ) ;
#2584=( LENGTH_UNIT ( ) NAMED_UNIT ( * ) SI_UNIT ( .MILLI., .METRE. ) );
#2592=ORIENTED_EDGE ( 'NONE', *, *, #273, .F. ) ;
#2608=DIRECTION ( 'NONE',  ( -1.000000000000000000, 0.000000000000000000, 0.000000000000000000 ) ) ;
#2611=VECTOR ( 'NONE', #3909, 1000.000000000000000 ) ;
#2616=CARTESIAN_POINT ( 'NONE',  ( -36.78095584970496645, 12.70544120911856290, 0.000000000000000000 ) ) ;
#2619=VECTOR ( 'NONE', #165, 1000.000000000000000 ) ;
#2626=CARTESIAN_POINT ( 'NONE',  ( 47.36967921662626679, 6.904171036223937463, 12.50000000000000000 ) ) ;
#2631=ADVANCED_FACE ( 'NONE', ( #3371 ), #5744, .F. ) ;
#2644=VECTOR ( 'NONE', #5436, 1000.000000000000000 ) ;
#2655=ADVANCED_FACE ( 'NONE', ( #2365 ), #7187, .F. ) ;
#2662=DIRECTION ( 'NONE',  ( -0.000000000000000000, -0.000000000000000000, -1.000000000000000000 ) ) ;
#2670=CARTESIAN_POINT ( 'NONE',  ( -49.28095584970496645, 12.70544120911856112, 12.50000000000000000 ) ) ;
#2693=DIRECTION ( 'NONE',  ( -0.000000000000000000, 0.000000000000000000, 1.000000000000000000 ) ) ;
#2705=LINE ( 'NONE', #856, #6234 ) ;
#2708=FACE_OUTER_BOUND ( 'NONE', #5577, .T. ) ;
#2743=LINE ( 'NONE', #1415, #6256 ) ;
#2744=ORIENTED_EDGE ( 'NONE', *, *, #855, .T. ) ;
#2789=DIRECTION ( 'NONE',  ( -0.000000000000000000, 0.000000000000000000, 1.000000000000000000 ) ) ;
#2790=FACE_BOUND ( 'NONE', #3191, .T. ) ;
#2791=ORIENTED_EDGE ( 'NONE', *, *, #5682, .T. ) ;
#2806=EDGE_CURVE ( 'NONE', #3331, #308, #6022, .T. ) ;
#2814=CARTESIAN_POINT ( 'NONE',  ( -0.000000000000000000, -5.595828947448873159, 0.000000000000000000 ) ) ;
#2819=DIRECTION ( 'NONE',  ( -0.000000000000000000, -0.000000000000000000, -1.000000000000000000 ) ) ;
#2842=CARTESIAN_POINT ( 'NONE',  ( 0.7190441502950353225, 62.70544120911855401, 12.50000000000000000 ) ) ;
#2855=FACE_OUTER_BOUND ( 'NONE', #4520, .T. ) ;
#2866=DIRECTION ( 'NONE',  ( -0.000000000000000000, 0.000000000000000000, 1.000000000000000000 ) ) ;
#2869=DIRECTION ( 'NONE',  ( -0.5000000000000004441, -0.8660254037844383745, 0.000000000000000000 ) ) ;
#2871=FACE_BOUND ( 'NONE', #5231, .T. ) ;
#2873=PRODUCT_DEFINITION_CONTEXT ( 'detailed design', #244, 'design' ) ;
#2874=CIRCLE ( 'NONE', #3891, 12.50000000000000355 ) ;
#2920=ORIENTED_EDGE ( 'NONE', *, *, #1349, .T. ) ;
#2931=ORIENTED_EDGE ( 'NONE', *, *, #5766, .T. ) ;
#2955=CARTESIAN_POINT ( 'NONE',  ( -49.28095584970496645, -62.29455879088143888, 12.50000000000000000 ) ) ;
#2957=DIRECTION ( 'NONE',  ( 0.5000000000000004441, 0.8660254037844383745, 0.000000000000000000 ) ) ;
#2961=ORIENTED_EDGE ( 'NONE', *, *, #3513, .T. ) ;
#2966=VERTEX_POINT ( 'NONE', #7052 ) ;
#2969=DIRECTION ( 'NONE',  ( -0.000000000000000000, 0.000000000000000000, 1.000000000000000000 ) ) ;
#3011=CARTESIAN_POINT ( 'NONE',  ( 25.71904415029483459, 19.40417101989674009, 0.000000000000000000 ) ) ;
#3016=VECTOR ( 'NONE', #326, 1000.000000000000000 ) ;
#3023=CARTESIAN_POINT ( 'NONE',  ( -49.28095584970496645, -62.29455879088143888, 0.000000000000000000 ) ) ;
#3036=EDGE_LOOP ( 'NONE', ( #3767, #1703, #6937, #5970 ) ) ;
#3037=AXIS2_PLACEMENT_3D ( 'NONE', #4032, #6486, #391 ) ;
#3050=FACE_OUTER_BOUND ( 'NONE', #1239, .T. ) ;
#3060=VECTOR ( 'NONE', #2294, 1000.000000000000000 ) ;
#3062=ORIENTED_EDGE ( 'NONE', *, *, #5526, .F. ) ;
#3084=( LENGTH_UNIT ( ) NAMED_UNIT ( * ) SI_UNIT ( .MILLI., .METRE. ) );
#3095=DIRECTION ( 'NONE',  ( -0.000000000000000000, -0.000000000000000000, -1.000000000000000000 ) ) ;
#3097=( GEOMETRIC_REPRESENTATION_CONTEXT ( 3 ) GLOBAL_UNCERTAINTY_ASSIGNED_CONTEXT ( ( #3838 ) ) GLOBAL_UNIT_ASSIGNED_CONTEXT ( ( #2584, #4375, #6834 ) ) REPRESENTATION_CONTEXT ( 'NONE', 'WORKASPACE' ) );
#3098=ORIENTED_EDGE ( 'NONE', *, *, #2806, .T. ) ;
#3102=EDGE_CURVE ( 'NONE', #334, #5922, #1070, .T. ) ;
#3111=CARTESIAN_POINT ( 'NONE',  ( -16.96112411586215529, 80.38061160285559481, 0.000000000000000000 ) ) ;
#3131=LINE ( 'NONE', #1832, #3561 ) ;
#3145=CIRCLE ( 'NONE', #5706, 12.50000000000001776 ) ;
#3172=AXIS2_PLACEMENT_3D ( 'NONE', #3499, #7268, #3538 ) ;
#3178=ADVANCED_FACE ( 'NONE', ( #3601 ), #7846, .F. ) ;
#3185=AXIS2_PLACEMENT_3D ( 'NONE', #2020, #2182, #6922 ) ;
#3191=EDGE_LOOP ( 'NONE', ( #879, #4062 ) ) ;
#3195=FACE_OUTER_BOUND ( 'NONE', #3405, .T. ) ;
#3223=DIRECTION ( 'NONE',  ( -0.000000000000000000, -0.000000000000000000, -1.000000000000000000 ) ) ;
#3249=CARTESIAN_POINT ( 'NONE',  ( -24.28095581706361372, 2.657566677470048251E-15, 12.50000000000000000 ) ) ;
#3277=DIRECTION ( 'NONE',  ( -0.000000000000000000, 0.000000000000000000, 1.000000000000000000 ) ) ;
#3283=PRODUCT_DEFINITION_SHAPE ( 'NONE', 'NONE',  #3552 ) ;
#3292=ORIENTED_EDGE ( 'NONE', *, *, #5020, .F. ) ;
#3319=DIRECTION ( 'NONE',  ( 1.000000000000000000, 0.000000000000000000, 0.000000000000000000 ) ) ;
#3320=ORIENTED_EDGE ( 'NONE', *, *, #1303, .F. ) ;
#3331=VERTEX_POINT ( 'NONE', #3686 ) ;
#3338=EDGE_CURVE ( 'NONE', #5747, #2966, #1908, .T. ) ;
#3339=CARTESIAN_POINT ( 'NONE',  ( -49.28095584970496645, -62.29455879088143888, 12.50000000000000000 ) ) ;
#3341=DIRECTION ( 'NONE',  ( -1.000000000000000000, 0.000000000000000000, 0.000000000000000000 ) ) ;
#3367=ORIENTED_EDGE ( 'NONE', *, *, #669, .F. ) ;
#3371=FACE_OUTER_BOUND ( 'NONE', #2316, .T. ) ;
#3376=PLANE ( 'NONE',  #5441 ) ;
#3389=VERTEX_POINT ( 'NONE', #6767 ) ;
#3390=AXIS2_PLACEMENT_3D ( 'NONE', #5818, #6945, #7581 ) ;
#3392=VECTOR ( 'NONE', #3341, 1000.000000000000000 ) ;
#3399=CARTESIAN_POINT ( 'NONE',  ( -49.28095584970496645, -62.29455879088143888, 12.50000000000000000 ) ) ;
#3405=EDGE_LOOP ( 'NONE', ( #6495, #3462, #6195, #3098 ) ) ;
#3412=EDGE_CURVE ( 'NONE', #3331, #6641, #5322, .T. ) ;
#3414=EDGE_CURVE ( 'NONE', #5929, #1336, #1474, .T. ) ;
#3440=ORIENTED_EDGE ( 'NONE', *, *, #669, .T. ) ;
#3462=ORIENTED_EDGE ( 'NONE', *, *, #7079, .F. ) ;
#3463=ORIENTED_EDGE ( 'NONE', *, *, #4478, .T. ) ;
#3471=CARTESIAN_POINT ( 'NONE',  ( -24.28095581706361727, -30.59582894744887582, 12.50000000000000000 ) ) ;
#3477=FACE_BOUND ( 'NONE', #5533, .T. ) ;
#3481=ORIENTED_EDGE ( 'NONE', *, *, #6756, .F. ) ;
#3489=ORIENTED_EDGE ( 'NONE', *, *, #2806, .F. ) ;
#3490=DIRECTION ( 'NONE',  ( -1.000000000000000000, 0.000000000000000000, 0.000000000000000000 ) ) ;
#3499=CARTESIAN_POINT ( 'NONE',  ( 0.000000000000000000, 0.000000000000000000, 0.000000000000000000 ) ) ;
#3500=DIRECTION ( 'NONE',  ( -1.000000000000000000, 0.000000000000000000, 0.000000000000000000 ) ) ;
#3506=AXIS2_PLACEMENT_3D ( 'NONE', #3558, #4832, #4075 ) ;
#3513=EDGE_CURVE ( 'NONE', #5007, #7081, #1855, .T. ) ;
#3518=ORIENTED_EDGE ( 'NONE', *, *, #7912, .T. ) ;
#3536=ORIENTED_EDGE ( 'NONE', *, *, #4478, .F. ) ;
#3538=DIRECTION ( 'NONE',  ( 1.000000000000000000, 0.000000000000000000, 0.000000000000000000 ) ) ;
#3547=CARTESIAN_POINT ( 'NONE',  ( 32.53766565774834163, -18.78563002630307111, 0.000000000000000000 ) ) ;
#3552=PRODUCT_DEFINITION ( 'UNKNOWN', '', #1684, #2873 ) ;
#3558=CARTESIAN_POINT ( 'NONE',  ( 25.71904415029483459, 19.40417101989674009, 0.000000000000000000 ) ) ;
#3561=VECTOR ( 'NONE', #6175, 1000.000000000000000 ) ;
#3589=DIRECTION ( 'NONE',  ( 1.000000000000000000, 0.000000000000000000, 0.000000000000000000 ) ) ;
#3601=FACE_OUTER_BOUND ( 'NONE', #5246, .T. ) ;
#3602=ORIENTED_EDGE ( 'NONE', *, *, #7686, .T. ) ;
#3605=ORIENTED_EDGE ( 'NONE', *, *, #276, .T. ) ;
#3620=LINE ( 'NONE', #2532, #5275 ) ;
#3622=DIRECTION ( 'NONE',  ( -0.000000000000000000, 0.000000000000000000, 1.000000000000000000 ) ) ;
#3654=ORIENTED_EDGE ( 'NONE', *, *, #3338, .T. ) ;
#3660=DIRECTION ( 'NONE',  ( -0.000000000000000000, 0.000000000000000000, 1.000000000000000000 ) ) ;
#3686=CARTESIAN_POINT ( 'NONE',  ( 0.7190441502950353225, 87.70544117646394966, 12.50000000000000000 ) ) ;
#3690=AXIS2_PLACEMENT_3D ( 'NONE', #3339, #2819, #5788 ) ;
#3709=VECTOR ( 'NONE', #7357, 1000.000000000000000 ) ;
#3716=CARTESIAN_POINT ( 'NONE',  ( 38.21904415029501934, 62.70544120911855401, 0.000000000000000000 ) ) ;
#3723=( NAMED_UNIT ( * ) SI_UNIT ( $, .STERADIAN. ) SOLID_ANGLE_UNIT ( ) );
#3736=VERTEX_POINT ( 'NONE', #601 ) ;
#3737=DIRECTION ( 'NONE',  ( -0.000000000000000000, 0.000000000000000000, 1.000000000000000000 ) ) ;
#3752=LINE ( 'NONE', #849, #2619 ) ;
#3767=ORIENTED_EDGE ( 'NONE', *, *, #4293, .F. ) ;
#3779=AXIS2_PLACEMENT_3D ( 'NONE', #383, #1502, #2273 ) ;
#3781=DIRECTION ( 'NONE',  ( -0.000000000000000000, 0.000000000000000000, 1.000000000000000000 ) ) ;
#3788=CARTESIAN_POINT ( 'NONE',  ( 38.21904415029484170, 19.40417101989674009, 12.50000000000000000 ) ) ;
#3796=DIRECTION ( 'NONE',  ( 1.000000000000000000, 0.000000000000000000, 0.000000000000000000 ) ) ;
#3817=FACE_OUTER_BOUND ( 'NONE', #6401, .T. ) ;
#3820=DIRECTION ( 'NONE',  ( -0.000000000000000000, -0.000000000000000000, -1.000000000000000000 ) ) ;
#3838=UNCERTAINTY_MEASURE_WITH_UNIT (LENGTH_MEASURE( 1.000000000000000082E-05 ), #2584, 'distance_accuracy_value', 'NONE');
#3886=CARTESIAN_POINT ( 'NONE',  ( 50.71904415029504065, 62.70544120911855401, 0.000000000000000000 ) ) ;
#3891=AXIS2_PLACEMENT_3D ( 'NONE', #5679, #5519, #4266 ) ;
#3899=EDGE_CURVE ( 'NONE', #7081, #5007, #6611, .T. ) ;
#3909=DIRECTION ( 'NONE',  ( -0.000000000000000000, -0.000000000000000000, -1.000000000000000000 ) ) ;
#3915=CARTESIAN_POINT ( 'NONE',  ( 0.7190441502950353225, 62.70544120911855401, 0.000000000000000000 ) ) ;
#3918=ORIENTED_EDGE ( 'NONE', *, *, #6756, .T. ) ;
#3924=DIRECTION ( 'NONE',  ( -0.000000000000000000, -0.000000000000000000, -1.000000000000000000 ) ) ;
#3925=ORIENTED_EDGE ( 'NONE', *, *, #7553, .T. ) ;
#3933=ORIENTED_EDGE ( 'NONE', *, *, #276, .F. ) ;
#3941=EDGE_LOOP ( 'NONE', ( #6883, #1990 ) ) ;
#3945=ADVANCED_FACE ( 'NONE', ( #4709 ), #2236, .F. ) ;
#3955=ORIENTED_EDGE ( 'NONE', *, *, #5862, .F. ) ;
#3956=DIRECTION ( 'NONE',  ( -0.000000000000000000, 0.000000000000000000, 1.000000000000000000 ) ) ;
#3970=DIRECTION ( 'NONE',  ( -1.000000000000000000, 1.094506615593124476E-16, 0.000000000000000000 ) ) ;
#3971=CARTESIAN_POINT ( 'NONE',  ( -48.67326389759909944, 48.65950482248330644, 0.000000000000000000 ) ) ;
#3975=DIRECTION ( 'NONE',  ( -1.000000000000000000, 0.000000000000000000, 0.000000000000000000 ) ) ;
#3977=CARTESIAN_POINT ( 'NONE',  ( 50.71904415029504065, 62.70544120911855401, 12.50000000000000000 ) ) ;
#3986=EDGE_CURVE ( 'NONE', #52, #6264, #7261, .T. ) ;
#3991=DIRECTION ( 'NONE',  ( -0.000000000000000000, 0.000000000000000000, 1.000000000000000000 ) ) ;
#4008=CARTESIAN_POINT ( 'NONE',  ( 0.000000000000000000, 87.70544117646394966, 12.50000000000000000 ) ) ;
#4032=CARTESIAN_POINT ( 'NONE',  ( 0.7190441502950353225, 62.70544120911855401, 12.50000000000000000 ) ) ;
#4034=MANIFOLD_SOLID_BREP ( 'Yükseklik-Ekstrüzyon1', #7600 ) ;
#4049=DIRECTION ( 'NONE',  ( -1.000000000000000000, 0.000000000000000000, 0.000000000000000000 ) ) ;
#4050=EDGE_CURVE ( 'NONE', #7362, #6044, #4228, .T. ) ;
#4051=MECHANICAL_DESIGN_GEOMETRIC_PRESENTATION_REPRESENTATION('',(#7383),#5592);
#4062=ORIENTED_EDGE ( 'NONE', *, *, #6944, .F. ) ;
#4064=CARTESIAN_POINT ( 'NONE',  ( -61.78095584970497356, 12.70544120911856112, 0.000000000000000000 ) ) ;
#4065=DIRECTION ( 'NONE',  ( -0.000000000000000000, -0.000000000000000000, -1.000000000000000000 ) ) ;
#4075=DIRECTION ( 'NONE',  ( 1.000000000000000000, 0.000000000000000000, 0.000000000000000000 ) ) ;
#4081=CARTESIAN_POINT ( 'NONE',  ( 0.7190441502950353225, 62.70544120911855401, 12.50000000000000000 ) ) ;
#4087=CARTESIAN_POINT ( 'NONE',  ( -49.28095584970496645, -62.29455879088143888, 12.50000000000000000 ) ) ;
#4093=FACE_BOUND ( 'NONE', #4562, .T. ) ;
#4094=FACE_OUTER_BOUND ( 'NONE', #548, .T. ) ;
#4107=EDGE_CURVE ( 'NONE', #5527, #5402, #19, .T. ) ;
#4110=CARTESIAN_POINT ( 'NONE',  ( 0.000000000000000000, 0.000000000000000000, 0.000000000000000000 ) ) ;
#4128=FACE_BOUND ( 'NONE', #4503, .T. ) ;
#4133=DIRECTION ( 'NONE',  ( 1.000000000000000000, 0.000000000000000000, 0.000000000000000000 ) ) ;
#4147=ORIENTED_EDGE ( 'NONE', *, *, #3412, .T. ) ;
#4167=AXIS2_PLACEMENT_3D ( 'NONE', #2842, #3991, #7642 ) ;
#4169=FACE_BOUND ( 'NONE', #5529, .T. ) ;
#4178=CARTESIAN_POINT ( 'NONE',  ( -74.28095588234631919, 12.70544120911856112, 12.50000000000000000 ) ) ;
#4186=DIRECTION ( 'NONE',  ( 0.000000000000000000, 0.000000000000000000, 1.000000000000000000 ) ) ;
#4212=CARTESIAN_POINT ( 'NONE',  ( -11.78095584970496290, 62.70544120911855401, 12.50000000000000000 ) ) ;
#4213=DIRECTION ( 'NONE',  ( 1.000000000000000000, 0.000000000000000000, 0.000000000000000000 ) ) ;
#4228=LINE ( 'NONE', #5479, #2644 ) ;
#4242=DIRECTION ( 'NONE',  ( -1.000000000000000000, 0.000000000000000000, 0.000000000000000000 ) ) ;
#4263=ORIENTED_EDGE ( 'NONE', *, *, #5910, .F. ) ;
#4265=DIRECTION ( 'NONE',  ( 0.7070068166729618353, 0.7072067315700302226, 0.000000000000000000 ) ) ;
#4266=DIRECTION ( 'NONE',  ( 1.000000000000000000, 0.000000000000000000, 0.000000000000000000 ) ) ;
#4289=LINE ( 'NONE', #4212, #1889 ) ;
#4293=EDGE_CURVE ( 'NONE', #819, #1936, #2705, .T. ) ;
#4309=DIRECTION ( 'NONE',  ( -0.7072067315700303336, 0.7070068166729619463, 0.000000000000000000 ) ) ;
#4310=CYLINDRICAL_SURFACE ( 'NONE', #448, 24.99999998367932719 ) ;
#4330=AXIS2_PLACEMENT_3D ( 'NONE', #5794, #6918, #2137 ) ;
#4353=CARTESIAN_POINT ( 'NONE',  ( 38.21904415029484170, 19.40417101989674009, 12.50000000000000000 ) ) ;
#4359=EDGE_CURVE ( 'NONE', #5929, #3389, #5875, .T. ) ;
#4364=DIRECTION ( 'NONE',  ( 0.000000000000000000, 1.000000000000000000, -0.000000000000000000 ) ) ;
#4375=( NAMED_UNIT ( * ) PLANE_ANGLE_UNIT ( ) SI_UNIT ( $, .RADIAN. ) );
#4385=ORIENTED_EDGE ( 'NONE', *, *, #251, .T. ) ;
#4426=VECTOR ( 'NONE', #4866, 1000.000000000000000 ) ;
#4438=ORIENTED_EDGE ( 'NONE', *, *, #6757, .T. ) ;
#4472=ORIENTED_EDGE ( 'NONE', *, *, #7246, .T. ) ;
#4478=EDGE_CURVE ( 'NONE', #1918, #7209, #212, .T. ) ;
#4483=VERTEX_POINT ( 'NONE', #88 ) ;
#4497=CARTESIAN_POINT ( 'NONE',  ( -74.28095588234631919, -62.29455879088143888, 0.000000000000000000 ) ) ;
#4503=EDGE_LOOP ( 'NONE', ( #2920, #1060 ) ) ;
#4520=EDGE_LOOP ( 'NONE', ( #2390, #522, #3463, #5396 ) ) ;
#4530=AXIS2_PLACEMENT_3D ( 'NONE', #652, #3781, #7546 ) ;
#4539=CIRCLE ( 'NONE', #2366, 12.50000000000000355 ) ;
#4544=AXIS2_PLACEMENT_3D ( 'NONE', #3977, #5947, #2133 ) ;
#4562=EDGE_LOOP ( 'NONE', ( #7890, #713 ) ) ;
#4575=AXIS2_PLACEMENT_3D ( 'NONE', #7142, #1561, #962 ) ;
#4586=ORIENTED_EDGE ( 'NONE', *, *, #1066, .T. ) ;
#4599=ORIENTED_EDGE ( 'NONE', *, *, #273, .T. ) ;
#4625=EDGE_CURVE ( 'NONE', #3331, #1336, #1606, .T. ) ;
#4630=ADVANCED_FACE ( 'NONE', ( #2049 ), #5208, .T. ) ;
#4631=ORIENTED_EDGE ( 'NONE', *, *, #3513, .F. ) ;
#4642=CYLINDRICAL_SURFACE ( 'NONE', #5213, 12.50000000000000355 ) ;
#4643=FACE_OUTER_BOUND ( 'NONE', #3036, .T. ) ;
#4662=VECTOR ( 'NONE', #284, 1000.000000000000114 ) ;
#4683=DIRECTION ( 'NONE',  ( -1.000000000000000000, 0.000000000000000000, 0.000000000000000000 ) ) ;
#4689=PLANE ( 'NONE',  #6626 ) ;
#4707=AXIS2_PLACEMENT_3D ( 'NONE', #4994, #2509, #4906 ) ;
#4708=EDGE_LOOP ( 'NONE', ( #795, #4263, #3481, #7174 ) ) ;
#4709=FACE_OUTER_BOUND ( 'NONE', #7255, .T. ) ;
#4727=ORIENTED_EDGE ( 'NONE', *, *, #6944, .T. ) ;
#4747=AXIS2_PLACEMENT_3D ( 'NONE', #2149, #7047, #1424 ) ;
#4750=ADVANCED_FACE ( 'NONE', ( #5414 ), #6581, .T. ) ;
#4771=EDGE_CURVE ( 'NONE', #6738, #2966, #730, .T. ) ;
#4773=CARTESIAN_POINT ( 'NONE',  ( 0.7190441666157093570, -30.59582893112819946, 0.000000000000000000 ) ) ;
#4778=LINE ( 'NONE', #3547, #7915 ) ;
#4802=DIRECTION ( 'NONE',  ( -1.000000000000000000, 0.000000000000000000, 0.000000000000000000 ) ) ;
#4806=EDGE_LOOP ( 'NONE', ( #3955, #6007, #3925, #3062 ) ) ;
#4817=ADVANCED_FACE ( 'NONE', ( #2259 ), #4689, .T. ) ;
#4820=DIRECTION ( 'NONE',  ( -1.000000000000000000, 0.000000000000000000, 0.000000000000000000 ) ) ;
#4822=ORIENTED_EDGE ( 'NONE', *, *, #3414, .F. ) ;
#4823=ADVANCED_FACE ( 'NONE', ( #1652, #4093, #4128, #6546, #4169, #1047 ), #6027, .F. ) ;
#4832=DIRECTION ( 'NONE',  ( -0.000000000000000000, 0.000000000000000000, 1.000000000000000000 ) ) ;
#4845=VECTOR ( 'NONE', #3223, 1000.000000000000000 ) ;
#4848=VECTOR ( 'NONE', #3924, 1000.000000000000000 ) ;
#4861=CARTESIAN_POINT ( 'NONE',  ( -24.28095581706361727, -30.59582894744887582, 12.50000000000000000 ) ) ;
#4866=DIRECTION ( 'NONE',  ( -0.000000000000000000, -0.000000000000000000, -1.000000000000000000 ) ) ;
#4869=DIRECTION ( 'NONE',  ( -0.000000000000000000, -0.000000000000000000, -1.000000000000000000 ) ) ;
#4871=AXIS2_PLACEMENT_3D ( 'NONE', #1580, #3277, #227 ) ;
#4899=DIRECTION ( 'NONE',  ( -0.000000000000000000, -0.000000000000000000, -1.000000000000000000 ) ) ;
#4900=CIRCLE ( 'NONE', #5150, 24.99999996734539920 ) ;
#4904=ORIENTED_EDGE ( 'NONE', *, *, #3899, .F. ) ;
#4906=DIRECTION ( 'NONE',  ( 0.000000000000000000, 0.000000000000000000, 1.000000000000000000 ) ) ;
#4907=CARTESIAN_POINT ( 'NONE',  ( -48.67326389759909944, 48.65950482248330644, 12.50000000000000000 ) ) ;
#4921=CARTESIAN_POINT ( 'NONE',  ( -66.45428044951677293, 30.87346046883880035, 0.000000000000000000 ) ) ;
#4928=AXIS2_PLACEMENT_3D ( 'NONE', #1384, #1658, #6283 ) ;
#4943=APPLICATION_CONTEXT ( 'automotive_design' ) ;
#4963=AXIS2_PLACEMENT_3D ( 'NONE', #3249, #3970, #2121 ) ;
#4982=SHAPE_DEFINITION_REPRESENTATION ( #3283, #6180 ) ;
#4994=CARTESIAN_POINT ( 'NONE',  ( -74.28095588234631919, 0.000000000000000000, 12.50000000000000000 ) ) ;
#5001=VERTEX_POINT ( 'NONE', #6820 ) ;
#5007=VERTEX_POINT ( 'NONE', #1840 ) ;
#5020=EDGE_CURVE ( 'NONE', #7081, #5902, #4289, .T. ) ;
#5026=EDGE_CURVE ( 'NONE', #869, #2966, #1321, .T. ) ;
#5040=CIRCLE ( 'NONE', #1452, 12.50000000000001776 ) ;
#5054=CARTESIAN_POINT ( 'NONE',  ( 72.36967921662629522, 50.20544122544588816, 12.50000000000000000 ) ) ;
#5057=ORIENTED_EDGE ( 'NONE', *, *, #7686, .F. ) ;
#5077=CARTESIAN_POINT ( 'NONE',  ( 25.71904415029483459, 19.40417101989674009, 12.50000000000000000 ) ) ;
#5101=CIRCLE ( 'NONE', #6140, 25.00000003264134918 ) ;
#5108=DIRECTION ( 'NONE',  ( -0.000000000000000000, 0.000000000000000000, 1.000000000000000000 ) ) ;
#5127=ORIENTED_EDGE ( 'NONE', *, *, #2053, .T. ) ;
#5135=CARTESIAN_POINT ( 'NONE',  ( -16.96112411586215529, 80.38061160285559481, 12.50000000000000000 ) ) ;
#5139=LINE ( 'NONE', #2626, #2611 ) ;
#5150=AXIS2_PLACEMENT_3D ( 'NONE', #3886, #882, #5202 ) ;
#5153=ORIENTED_EDGE ( 'NONE', *, *, #1303, .T. ) ;
#5159=DIRECTION ( 'NONE',  ( 1.000000000000000000, 0.000000000000000000, 0.000000000000000000 ) ) ;
#5164=VECTOR ( 'NONE', #5663, 1000.000000000000000 ) ;
#5166=AXIS2_PLACEMENT_3D ( 'NONE', #1906, #818, #705 ) ;
#5169=LINE ( 'NONE', #5054, #3016 ) ;
#5179=DIRECTION ( 'NONE',  ( -0.000000000000000000, -0.000000000000000000, -1.000000000000000000 ) ) ;
#5182=CARTESIAN_POINT ( 'NONE',  ( 50.71904415029504065, 62.70544120911855401, 12.50000000000000000 ) ) ;
#5202=DIRECTION ( 'NONE',  ( 1.000000000000000000, 0.000000000000000000, 0.000000000000000000 ) ) ;
#5208=CYLINDRICAL_SURFACE ( 'NONE', #3690, 25.00000003264134918 ) ;
#5213=AXIS2_PLACEMENT_3D ( 'NONE', #4087, #3095, #4242 ) ;
#5217=DIRECTION ( 'NONE',  ( 1.000000000000000000, 0.000000000000000000, 0.000000000000000000 ) ) ;
#5225=PLANE ( 'NONE',  #3779 ) ;
#5231=EDGE_LOOP ( 'NONE', ( #4904, #4631 ) ) ;
#5246=EDGE_LOOP ( 'NONE', ( #7460, #434, #6314, #565 ) ) ;
#5275=VECTOR ( 'NONE', #6824, 1000.000000000000000 ) ;
#5285=ORIENTED_EDGE ( 'NONE', *, *, #5391, .T. ) ;
#5300=CIRCLE ( 'NONE', #5702, 12.50000000000000355 ) ;
#5302=DIRECTION ( 'NONE',  ( 1.000000000000000000, 0.000000000000000000, 0.000000000000000000 ) ) ;
#5308=ORIENTED_EDGE ( 'NONE', *, *, #2498, .F. ) ;
#5322=CIRCLE ( 'NONE', #4928, 24.99999996734539920 ) ;
#5333=DIRECTION ( 'NONE',  ( -0.000000000000000000, -0.000000000000000000, -1.000000000000000000 ) ) ;
#5345=ADVANCED_FACE ( 'NONE', ( #7253 ), #7326, .T. ) ;
#5373=ORIENTED_EDGE ( 'NONE', *, *, #4050, .T. ) ;
#5391=EDGE_CURVE ( 'NONE', #1141, #6641, #1228, .T. ) ;
#5394=VECTOR ( 'NONE', #2190, 1000.000000000000000 ) ;
#5396=ORIENTED_EDGE ( 'NONE', *, *, #5910, .T. ) ;
#5402=VERTEX_POINT ( 'NONE', #6880 ) ;
#5404=ORIENTED_EDGE ( 'NONE', *, *, #2548, .T. ) ;
#5414=FACE_OUTER_BOUND ( 'NONE', #999, .T. ) ;
#5416=CARTESIAN_POINT ( 'NONE',  ( 13.21904415029483459, 19.40417101989674009, 12.50000000000000000 ) ) ;
#5424=CIRCLE ( 'NONE', #1962, 12.50000000000001776 ) ;
#5426=CYLINDRICAL_SURFACE ( 'NONE', #5820, 12.50000000000000355 ) ;
#5433=ORIENTED_EDGE ( 'NONE', *, *, #7784, .T. ) ;
#5436=DIRECTION ( 'NONE',  ( -0.000000000000000000, -0.000000000000000000, -1.000000000000000000 ) ) ;
#5441=AXIS2_PLACEMENT_3D ( 'NONE', #1445, #255, #807 ) ;
#5448=ADVANCED_FACE ( 'NONE', ( #3195 ), #6199, .T. ) ;
#5462=CARTESIAN_POINT ( 'NONE',  ( -66.45428044951677293, 30.87346046883880035, 12.50000000000000000 ) ) ;
#5479=CARTESIAN_POINT ( 'NONE',  ( 25.71904415029483459, -5.595828947448873159, 12.50000000000000000 ) ) ;
#5488=ORIENTED_EDGE ( 'NONE', *, *, #3102, .F. ) ;
#5490=ORIENTED_EDGE ( 'NONE', *, *, #1163, .F. ) ;
#5499=ORIENTED_EDGE ( 'NONE', *, *, #5766, .F. ) ;
#5500=ORIENTED_EDGE ( 'NONE', *, *, #4771, .T. ) ;
#5518=DIRECTION ( 'NONE',  ( -1.000000000000000000, 0.000000000000000000, 0.000000000000000000 ) ) ;
#5519=DIRECTION ( 'NONE',  ( -0.000000000000000000, 0.000000000000000000, 1.000000000000000000 ) ) ;
#5526=EDGE_CURVE ( 'NONE', #3736, #781, #7412, .T. ) ;
#5527=VERTEX_POINT ( 'NONE', #217 ) ;
#5529=EDGE_LOOP ( 'NONE', ( #5404, #4385 ) ) ;
#5533=EDGE_LOOP ( 'NONE', ( #2592, #6421 ) ) ;
#5546=LINE ( 'NONE', #4861, #3709 ) ;
#5570=DIRECTION ( 'NONE',  ( 1.000000000000000000, 0.000000000000000000, 0.000000000000000000 ) ) ;
#5577=EDGE_LOOP ( 'NONE', ( #5500, #5778, #464, #4438 ) ) ;
#5591=CARTESIAN_POINT ( 'NONE',  ( -11.78095584970496290, 62.70544120911855401, 0.000000000000000000 ) ) ;
#5592=( GEOMETRIC_REPRESENTATION_CONTEXT ( 3 ) GLOBAL_UNCERTAINTY_ASSIGNED_CONTEXT ( ( #638 ) ) GLOBAL_UNIT_ASSIGNED_CONTEXT ( ( #3084, #475, #3723 ) ) REPRESENTATION_CONTEXT ( 'NONE', 'WORKASPACE' ) );
#5597=AXIS2_PLACEMENT_3D ( 'NONE', #1892, #6827, #1295 ) ;
#5600=CARTESIAN_POINT ( 'NONE',  ( -48.67326389759909944, 48.65950482248330644, 12.50000000000000000 ) ) ;
#5630=AXIS2_PLACEMENT_3D ( 'NONE', #457, #1048, #3500 ) ;
#5639=LINE ( 'NONE', #5135, #365 ) ;
#5640=ORIENTED_EDGE ( 'NONE', *, *, #7251, .T. ) ;
#5656=EDGE_LOOP ( 'NONE', ( #2276, #7092 ) ) ;
#5661=ORIENTED_EDGE ( 'NONE', *, *, #2484, .F. ) ;
#5663=DIRECTION ( 'NONE',  ( -0.000000000000000000, -0.000000000000000000, -1.000000000000000000 ) ) ;
#5679=CARTESIAN_POINT ( 'NONE',  ( -49.28095584970496645, 12.70544120911856112, 0.000000000000000000 ) ) ;
#5682=EDGE_CURVE ( 'NONE', #7541, #5527, #1643, .T. ) ;
#5689=ORIENTED_EDGE ( 'NONE', *, *, #855, .F. ) ;
#5702=AXIS2_PLACEMENT_3D ( 'NONE', #966, #2693, #5159 ) ;
#5706=AXIS2_PLACEMENT_3D ( 'NONE', #2502, #2541, #7472 ) ;
#5744=CYLINDRICAL_SURFACE ( 'NONE', #3390, 12.50000000000000355 ) ;
#5747=VERTEX_POINT ( 'NONE', #4178 ) ;
#5750=CARTESIAN_POINT ( 'NONE',  ( -74.28095588234631919, -62.29455879088143888, 12.50000000000000000 ) ) ;
#5751=FACE_OUTER_BOUND ( 'NONE', #678, .T. ) ;
#5753=CIRCLE ( 'NONE', #4330, 12.50000000000000355 ) ;
#5766=EDGE_CURVE ( 'NONE', #1635, #4483, #4778, .T. ) ;
#5778=ORIENTED_EDGE ( 'NONE', *, *, #3338, .F. ) ;
#5785=AXIS2_PLACEMENT_3D ( 'NONE', #4110, #4186, #2351 ) ;
#5788=DIRECTION ( 'NONE',  ( -1.000000000000000000, 0.000000000000000000, 0.000000000000000000 ) ) ;
#5794=CARTESIAN_POINT ( 'NONE',  ( -49.28095584970496645, -62.29455879088143888, 0.000000000000000000 ) ) ;
#5801=VERTEX_POINT ( 'NONE', #4064 ) ;
#5804=ORIENTED_EDGE ( 'NONE', *, *, #6686, .T. ) ;
#5818=CARTESIAN_POINT ( 'NONE',  ( -49.28095584970496645, 12.70544120911856112, 12.50000000000000000 ) ) ;
#5820=AXIS2_PLACEMENT_3D ( 'NONE', #1025, #4065, #4820 ) ;
#5824=AXIS2_PLACEMENT_3D ( 'NONE', #6385, #6271, #3975 ) ;
#5862=EDGE_CURVE ( 'NONE', #2221, #3736, #2425, .T. ) ;
#5871=LINE ( 'NONE', #1732, #112 ) ;
#5875=LINE ( 'NONE', #2270, #852 ) ;
#5883=AXIS2_PLACEMENT_3D ( 'NONE', #3023, #2454, #39 ) ;
#5892=DIRECTION ( 'NONE',  ( 1.094506615593124353E-16, 1.000000000000000000, 0.000000000000000000 ) ) ;
#5902=VERTEX_POINT ( 'NONE', #5591 ) ;
#5910=EDGE_CURVE ( 'NONE', #7209, #5922, #5546, .T. ) ;
#5921=ORIENTED_EDGE ( 'NONE', *, *, #4359, .T. ) ;
#5922=VERTEX_POINT ( 'NONE', #47 ) ;
#5924=DIRECTION ( 'NONE',  ( 1.000000000000000000, 0.000000000000000000, 0.000000000000000000 ) ) ;
#5929=VERTEX_POINT ( 'NONE', #130 ) ;
#5939=CIRCLE ( 'NONE', #3506, 12.50000000000000355 ) ;
#5940=ORIENTED_EDGE ( 'NONE', *, *, #6711, .F. ) ;
#5947=DIRECTION ( 'NONE',  ( -0.000000000000000000, 0.000000000000000000, 1.000000000000000000 ) ) ;
#5970=ORIENTED_EDGE ( 'NONE', *, *, #251, .F. ) ;
#5973=EDGE_LOOP ( 'NONE', ( #7718, #1476, #2744, #1720 ) ) ;
#6007=ORIENTED_EDGE ( 'NONE', *, *, #2007, .T. ) ;
#6008=CARTESIAN_POINT ( 'NONE',  ( 50.71904415029504065, 62.70544120911855401, 12.50000000000000000 ) ) ;
#6022=LINE ( 'NONE', #527, #1220 ) ;
#6027=PLANE ( 'NONE',  #3172 ) ;
#6028=EDGE_CURVE ( 'NONE', #52, #869, #6343, .T. ) ;
#6044=VERTEX_POINT ( 'NONE', #6948 ) ;
#6050=DIRECTION ( 'NONE',  ( -1.000000000000000000, 0.000000000000000000, 0.000000000000000000 ) ) ;
#6056=CARTESIAN_POINT ( 'NONE',  ( 0.7190441502950353225, 62.70544120911855401, 0.000000000000000000 ) ) ;
#6063=CARTESIAN_POINT ( 'NONE',  ( 50.71904415029504065, 62.70544120911855401, 12.50000000000000000 ) ) ;
#6097=CARTESIAN_POINT ( 'NONE',  ( -66.45428044951677293, 30.87346046883880035, 12.50000000000000000 ) ) ;
#6124=CARTESIAN_POINT ( 'NONE',  ( -49.28095584970496645, 12.70544120911856112, 12.50000000000000000 ) ) ;
#6129=AXIS2_PLACEMENT_3D ( 'NONE', #2955, #6558, #3589 ) ;
#6140=AXIS2_PLACEMENT_3D ( 'NONE', #7834, #2866, #7672 ) ;
#6159=ORIENTED_EDGE ( 'NONE', *, *, #420, .T. ) ;
#6163=CARTESIAN_POINT ( 'NONE',  ( -24.28095581706362083, -62.29455879088143888, 0.000000000000000000 ) ) ;
#6175=DIRECTION ( 'NONE',  ( 1.094506615593124353E-16, 1.000000000000000000, 0.000000000000000000 ) ) ;
#6178=ORIENTED_EDGE ( 'NONE', *, *, #928, .T. ) ;
#6179=VERTEX_POINT ( 'NONE', #412 ) ;
#6180=SHAPE_REPRESENTATION ( 'Joint Plane', ( #5785 ), #3097 ) ;
#6195=ORIENTED_EDGE ( 'NONE', *, *, #3412, .F. ) ;
#6199=CYLINDRICAL_SURFACE ( 'NONE', #7657, 24.99999996734539920 ) ;
#6234=VECTOR ( 'NONE', #5179, 1000.000000000000000 ) ;
#6248=ORIENTED_EDGE ( 'NONE', *, *, #4293, .T. ) ;
#6256=VECTOR ( 'NONE', #2662, 1000.000000000000000 ) ;
#6264=VERTEX_POINT ( 'NONE', #2260 ) ;
#6268=AXIS2_PLACEMENT_3D ( 'NONE', #4081, #6538, #3490 ) ;
#6271=DIRECTION ( 'NONE',  ( -0.000000000000000000, -0.000000000000000000, -1.000000000000000000 ) ) ;
#6283=DIRECTION ( 'NONE',  ( 1.000000000000000000, 0.000000000000000000, 0.000000000000000000 ) ) ;
#6285=EDGE_LOOP ( 'NONE', ( #5308, #1935, #5285, #1353 ) ) ;
#6287=EDGE_LOOP ( 'NONE', ( #3605, #1572 ) ) ;
#6293=ADVANCED_FACE ( 'NONE', ( #4094 ), #6547, .F. ) ;
#6298=CARTESIAN_POINT ( 'NONE',  ( 50.71904415029504065, 87.70544117646394966, 12.50000000000000000 ) ) ;
#6307=LINE ( 'NONE', #1534, #3392 ) ;
#6309=EDGE_CURVE ( 'NONE', #7529, #5402, #754, .T. ) ;
#6314=ORIENTED_EDGE ( 'NONE', *, *, #1349, .F. ) ;
#6321=LINE ( 'NONE', #344, #5394 ) ;
#6343=LINE ( 'NONE', #5750, #4845 ) ;
#6361=DIRECTION ( 'NONE',  ( -0.000000000000000000, 0.000000000000000000, 1.000000000000000000 ) ) ;
#6385=CARTESIAN_POINT ( 'NONE',  ( 25.71904415029483459, 19.40417101989674009, 12.50000000000000000 ) ) ;
#6391=AXIS2_PLACEMENT_3D ( 'NONE', #6688, #2969, #6614 ) ;
#6401=EDGE_LOOP ( 'NONE', ( #3518, #6759, #6615, #5373 ) ) ;
#6405=CARTESIAN_POINT ( 'NONE',  ( -61.78095584970497356, 12.70544120911856112, 12.50000000000000000 ) ) ;
#6421=ORIENTED_EDGE ( 'NONE', *, *, #1553, .F. ) ;
#6449=CARTESIAN_POINT ( 'NONE',  ( -61.78095584970497356, -62.29455879088143888, 12.50000000000000000 ) ) ;
#6455=DIRECTION ( 'NONE',  ( 1.000000000000000000, 0.000000000000000000, 0.000000000000000000 ) ) ;
#6486=DIRECTION ( 'NONE',  ( -0.000000000000000000, -0.000000000000000000, -1.000000000000000000 ) ) ;
#6495=ORIENTED_EDGE ( 'NONE', *, *, #6816, .T. ) ;
#6501=CARTESIAN_POINT ( 'NONE',  ( -16.96112411586215529, 80.38061160285559481, 12.50000000000000000 ) ) ;
#6508=VECTOR ( 'NONE', #4364, 1000.000000000000000 ) ;
#6516=ADVANCED_FACE ( 'NONE', ( #7464 ), #1526, .F. ) ;
#6538=DIRECTION ( 'NONE',  ( -0.000000000000000000, -0.000000000000000000, -1.000000000000000000 ) ) ;
#6546=FACE_BOUND ( 'NONE', #6287, .T. ) ;
#6547=CYLINDRICAL_SURFACE ( 'NONE', #5630, 12.50000000000000000 ) ;
#6558=DIRECTION ( 'NONE',  ( -0.000000000000000000, 0.000000000000000000, 1.000000000000000000 ) ) ;
#6560=PLANE ( 'NONE',  #1087 ) ;
#6563=ORIENTED_EDGE ( 'NONE', *, *, #7864, .T. ) ;
#6567=ORIENTED_EDGE ( 'NONE', *, *, #5020, .T. ) ;
#6581=CYLINDRICAL_SURFACE ( 'NONE', #7270, 24.99999996734539209 ) ;
#6606=EDGE_CURVE ( 'NONE', #6264, #334, #404, .T. ) ;
#6611=CIRCLE ( 'NONE', #4167, 12.49999999999999822 ) ;
#6614=DIRECTION ( 'NONE',  ( 1.000000000000000000, 0.000000000000000000, 0.000000000000000000 ) ) ;
#6615=ORIENTED_EDGE ( 'NONE', *, *, #7864, .F. ) ;
#6626=AXIS2_PLACEMENT_3D ( 'NONE', #1688, #1203, #7151 ) ;
#6641=VERTEX_POINT ( 'NONE', #6501 ) ;
#6664=DIRECTION ( 'NONE',  ( -0.000000000000000000, -0.000000000000000000, -1.000000000000000000 ) ) ;
#6676=CIRCLE ( 'NONE', #4871, 24.99999996734560881 ) ;
#6686=EDGE_CURVE ( 'NONE', #6044, #7015, #445, .T. ) ;
#6688=CARTESIAN_POINT ( 'NONE',  ( -49.28095584970496645, -62.29455879088143888, 12.50000000000000000 ) ) ;
#6696=ORIENTED_EDGE ( 'NONE', *, *, #6309, .F. ) ;
#6704=CARTESIAN_POINT ( 'NONE',  ( 0.7190441502950353225, 62.70544120911855401, 12.50000000000000000 ) ) ;
#6711=EDGE_CURVE ( 'NONE', #869, #334, #6894, .T. ) ;
#6718=AXIS2_PLACEMENT_3D ( 'NONE', #7023, #1603, #4049 ) ;
#6719=PLANE ( 'NONE',  #575 ) ;
#6735=ADVANCED_FACE ( 'NONE', ( #7700 ), #4642, .F. ) ;
#6738=VERTEX_POINT ( 'NONE', #4921 ) ;
#6746=EDGE_CURVE ( 'NONE', #1386, #6179, #7532, .T. ) ;
#6756=EDGE_CURVE ( 'NONE', #6264, #7209, #3131, .T. ) ;
#6757=EDGE_CURVE ( 'NONE', #1141, #6738, #2199, .T. ) ;
#6759=ORIENTED_EDGE ( 'NONE', *, *, #420, .F. ) ;
#6762=CARTESIAN_POINT ( 'NONE',  ( 0.7190441502950353225, 62.70544120911855401, 12.50000000000000000 ) ) ;
#6767=CARTESIAN_POINT ( 'NONE',  ( 47.36967921662626679, 6.904171036223937463, 12.50000000000000000 ) ) ;
#6772=CARTESIAN_POINT ( 'NONE',  ( -61.78095584970497356, -62.29455879088143888, 12.50000000000000000 ) ) ;
#6791=CARTESIAN_POINT ( 'NONE',  ( 63.21904415029505486, 62.70544120911855401, 12.50000000000000000 ) ) ;
#6797=ORIENTED_EDGE ( 'NONE', *, *, #6746, .F. ) ;
#6803=FACE_OUTER_BOUND ( 'NONE', #6285, .T. ) ;
#6816=EDGE_CURVE ( 'NONE', #308, #784, #1378, .T. ) ;
#6820=CARTESIAN_POINT ( 'NONE',  ( 13.21904415029503355, 62.70544120911855401, 0.000000000000000000 ) ) ;
#6824=DIRECTION ( 'NONE',  ( -0.000000000000000000, -0.000000000000000000, -1.000000000000000000 ) ) ;
#6827=DIRECTION ( 'NONE',  ( -0.000000000000000000, 0.000000000000000000, 1.000000000000000000 ) ) ;
#6834=( NAMED_UNIT ( * ) SI_UNIT ( $, .STERADIAN. ) SOLID_ANGLE_UNIT ( ) );
#6844=AXIS2_PLACEMENT_3D ( 'NONE', #6124, #141, #1939 ) ;
#6867=CARTESIAN_POINT ( 'NONE',  ( -61.78095584970497356, 12.70544120911856112, 12.50000000000000000 ) ) ;
#6880=CARTESIAN_POINT ( 'NONE',  ( -36.78095584970496645, -62.29455879088143888, 0.000000000000000000 ) ) ;
#6883=ORIENTED_EDGE ( 'NONE', *, *, #414, .F. ) ;
#6894=CIRCLE ( 'NONE', #4575, 25.00000003264134918 ) ;
#6918=DIRECTION ( 'NONE',  ( -0.000000000000000000, 0.000000000000000000, 1.000000000000000000 ) ) ;
#6922=DIRECTION ( 'NONE',  ( 1.000000000000000000, 0.000000000000000000, 0.000000000000000000 ) ) ;
#6924=CYLINDRICAL_SURFACE ( 'NONE', #5166, 25.00000003264134918 ) ;
#6933=PRODUCT ( 'Joint Plane', 'Joint Plane', '', ( #7276 ) ) ;
#6937=ORIENTED_EDGE ( 'NONE', *, *, #2484, .T. ) ;
#6944=EDGE_CURVE ( 'NONE', #7782, #7250, #2542, .T. ) ;
#6945=DIRECTION ( 'NONE',  ( -0.000000000000000000, -0.000000000000000000, -1.000000000000000000 ) ) ;
#6947=DIRECTION ( 'NONE',  ( 1.000000000000000000, 0.000000000000000000, 0.000000000000000000 ) ) ;
#6948=CARTESIAN_POINT ( 'NONE',  ( 25.71904415029483459, -5.595828947448873159, 0.000000000000000000 ) ) ;
#7001=ORIENTED_EDGE ( 'NONE', *, *, #4107, .T. ) ;
#7015=VERTEX_POINT ( 'NONE', #7132 ) ;
#7023=CARTESIAN_POINT ( 'NONE',  ( -49.28095584970496645, 12.70544120911856112, 12.50000000000000000 ) ) ;
#7030=FACE_OUTER_BOUND ( 'NONE', #1022, .T. ) ;
#7047=DIRECTION ( 'NONE',  ( -0.000000000000000000, 0.000000000000000000, 1.000000000000000000 ) ) ;
#7052=CARTESIAN_POINT ( 'NONE',  ( -74.28095588234631919, 12.70544120911856112, 0.000000000000000000 ) ) ;
#7077=FACE_BOUND ( 'NONE', #3941, .T. ) ;
#7079=EDGE_CURVE ( 'NONE', #6641, #784, #5639, .T. ) ;
#7081=VERTEX_POINT ( 'NONE', #893 ) ;
#7092=ORIENTED_EDGE ( 'NONE', *, *, #7148, .T. ) ;
#7132=CARTESIAN_POINT ( 'NONE',  ( 0.7190441502950423169, -5.595828947448873159, 0.000000000000000000 ) ) ;
#7135=EDGE_LOOP ( 'NONE', ( #3536, #5689, #6563, #7336, #2486, #7562, #4147, #1915, #4472, #629, #7441, #3918 ) ) ;
#7142=CARTESIAN_POINT ( 'NONE',  ( -49.28095584970496645, -62.29455879088143888, 0.000000000000000000 ) ) ;
#7148=EDGE_CURVE ( 'NONE', #5402, #7529, #5753, .T. ) ;
#7150=EDGE_CURVE ( 'NONE', #5007, #5001, #2743, .T. ) ;
#7151=DIRECTION ( 'NONE',  ( 0.000000000000000000, -0.000000000000000000, -1.000000000000000000 ) ) ;
#7165=FACE_OUTER_BOUND ( 'NONE', #2450, .T. ) ;
#7169=CIRCLE ( 'NONE', #2545, 24.99999998367932719 ) ;
#7174=ORIENTED_EDGE ( 'NONE', *, *, #6606, .T. ) ;
#7180=ORIENTED_EDGE ( 'NONE', *, *, #928, .F. ) ;
#7187=CYLINDRICAL_SURFACE ( 'NONE', #306, 12.50000000000001066 ) ;
#7190=EDGE_LOOP ( 'NONE', ( #5640, #5488, #5940, #1839, #2564, #211, #1272, #7242, #3320, #2931, #310, #5804 ) ) ;
#7194=LINE ( 'NONE', #5416, #146 ) ;
#7209=VERTEX_POINT ( 'NONE', #3471 ) ;
#7213=ORIENTED_EDGE ( 'NONE', *, *, #810, .T. ) ;
#7242=ORIENTED_EDGE ( 'NONE', *, *, #7264, .T. ) ;
#7244=VECTOR ( 'NONE', #5892, 1000.000000000000000 ) ;
#7246=EDGE_CURVE ( 'NONE', #1141, #5747, #5101, .T. ) ;
#7250=VERTEX_POINT ( 'NONE', #417 ) ;
#7251=EDGE_CURVE ( 'NONE', #7015, #5922, #7169, .T. ) ;
#7253=FACE_OUTER_BOUND ( 'NONE', #339, .T. ) ;
#7255=EDGE_LOOP ( 'NONE', ( #1455, #2961, #6567, #59 ) ) ;
#7261=CIRCLE ( 'NONE', #1483, 25.00000003264134918 ) ;
#7264=EDGE_CURVE ( 'NONE', #308, #1401, #5871, .T. ) ;
#7268=DIRECTION ( 'NONE',  ( -0.000000000000000000, 0.000000000000000000, 1.000000000000000000 ) ) ;
#7270=AXIS2_PLACEMENT_3D ( 'NONE', #6063, #1169, #1126 ) ;
#7276=PRODUCT_CONTEXT ( 'NONE', #4943, 'mechanical' ) ;
#7280=CARTESIAN_POINT ( 'NONE',  ( 32.53766565774834163, -18.78563002630307111, 12.50000000000000000 ) ) ;
#7304=DIRECTION ( 'NONE',  ( -0.000000000000000000, 0.000000000000000000, 1.000000000000000000 ) ) ;
#7326=PLANE ( 'NONE',  #4707 ) ;
#7336=ORIENTED_EDGE ( 'NONE', *, *, #4359, .F. ) ;
#7357=DIRECTION ( 'NONE',  ( -0.000000000000000000, -0.000000000000000000, -1.000000000000000000 ) ) ;
#7362=VERTEX_POINT ( 'NONE', #540 ) ;
#7383=STYLED_ITEM('',(#7948),#4034);
#7412=CIRCLE ( 'NONE', #3185, 12.50000000000001776 ) ;
#7427=CARTESIAN_POINT ( 'NONE',  ( -74.28095588234631919, 0.000000000000000000, 0.000000000000000000 ) ) ;
#7441=ORIENTED_EDGE ( 'NONE', *, *, #3986, .T. ) ;
#7460=ORIENTED_EDGE ( 'NONE', *, *, #414, .T. ) ;
#7464=FACE_OUTER_BOUND ( 'NONE', #4708, .T. ) ;
#7472=DIRECTION ( 'NONE',  ( 1.000000000000000000, 0.000000000000000000, 0.000000000000000000 ) ) ;
#7486=AXIS2_PLACEMENT_3D ( 'NONE', #83, #2534, #2608 ) ;
#7518=DIRECTION ( 'NONE',  ( 1.000000000000000000, 0.000000000000000000, 0.000000000000000000 ) ) ;
#7529=VERTEX_POINT ( 'NONE', #7733 ) ;
#7530=DIRECTION ( 'NONE',  ( 1.000000000000000000, 0.000000000000000000, 0.000000000000000000 ) ) ;
#7532=CIRCLE ( 'NONE', #1124, 12.50000000000000355 ) ;
#7541=VERTEX_POINT ( 'NONE', #6449 ) ;
#7546=DIRECTION ( 'NONE',  ( 1.000000000000000000, 0.000000000000000000, 0.000000000000000000 ) ) ;
#7553=EDGE_CURVE ( 'NONE', #2350, #781, #2076, .T. ) ;
#7562=ORIENTED_EDGE ( 'NONE', *, *, #4625, .F. ) ;
#7569=DIRECTION ( 'NONE',  ( -0.000000000000000000, 0.000000000000000000, 1.000000000000000000 ) ) ;
#7579=DIRECTION ( 'NONE',  ( -0.000000000000000000, 0.000000000000000000, 1.000000000000000000 ) ) ;
#7581=DIRECTION ( 'NONE',  ( -1.000000000000000000, 0.000000000000000000, 0.000000000000000000 ) ) ;
#7597=FACE_BOUND ( 'NONE', #2160, .T. ) ;
#7598=ORIENTED_EDGE ( 'NONE', *, *, #5026, .F. ) ;
#7600=CLOSED_SHELL ( 'NONE', ( #6735, #865, #3178, #7747, #2631, #1403, #4817, #2388, #1745, #4750, #903, #5448, #330, #1550, #5345, #4630, #2572, #3945, #2655, #6293, #6516, #528, #1709, #4823 ) ) ;
#7601=ORIENTED_EDGE ( 'NONE', *, *, #6711, .T. ) ;
#7615=ORIENTED_EDGE ( 'NONE', *, *, #4107, .F. ) ;
#7642=DIRECTION ( 'NONE',  ( 1.000000000000000000, 0.000000000000000000, 0.000000000000000000 ) ) ;
#7657=AXIS2_PLACEMENT_3D ( 'NONE', #6762, #701, #5518 ) ;
#7672=DIRECTION ( 'NONE',  ( 1.000000000000000000, 0.000000000000000000, 0.000000000000000000 ) ) ;
#7673=CIRCLE ( 'NONE', #6391, 12.50000000000000355 ) ;
#7686=EDGE_CURVE ( 'NONE', #5527, #7541, #7673, .T. ) ;
#7693=CARTESIAN_POINT ( 'NONE',  ( 38.21904415029502644, 62.70544120911855401, 12.50000000000000000 ) ) ;
#7694=AXIS2_PLACEMENT_3D ( 'NONE', #3915, #6361, #3319 ) ;
#7700=FACE_OUTER_BOUND ( 'NONE', #7840, .T. ) ;
#7718=ORIENTED_EDGE ( 'NONE', *, *, #6686, .F. ) ;
#7725=CARTESIAN_POINT ( 'NONE',  ( -74.28095588234631919, -62.29455879088143888, 12.50000000000000000 ) ) ;
#7732=CIRCLE ( 'NONE', #4530, 12.49999999999999822 ) ;
#7733=CARTESIAN_POINT ( 'NONE',  ( -61.78095584970497356, -62.29455879088143888, 0.000000000000000000 ) ) ;
#7739=CARTESIAN_POINT ( 'NONE',  ( 0.7190441666157093570, -30.59582893112819946, 12.50000000000000000 ) ) ;
#7747=ADVANCED_FACE ( 'NONE', ( #3050 ), #2360, .F. ) ;
#7782=VERTEX_POINT ( 'NONE', #4353 ) ;
#7784=EDGE_CURVE ( 'NONE', #7541, #7529, #108, .T. ) ;
#7797=VERTEX_POINT ( 'NONE', #6405 ) ;
#7834=CARTESIAN_POINT ( 'NONE',  ( -49.28095584970496645, 12.70544120911856112, 12.50000000000000000 ) ) ;
#7840=EDGE_LOOP ( 'NONE', ( #2791, #7001, #6696, #390 ) ) ;
#7845=ORIENTED_EDGE ( 'NONE', *, *, #3899, .T. ) ;
#7846=CYLINDRICAL_SURFACE ( 'NONE', #2257, 12.50000000000001066 ) ;
#7864=EDGE_CURVE ( 'NONE', #7362, #3389, #908, .T. ) ;
#7865=EDGE_CURVE ( 'NONE', #1918, #7015, #6321, .T. ) ;
#7890=ORIENTED_EDGE ( 'NONE', *, *, #6746, .T. ) ;
#7912=EDGE_CURVE ( 'NONE', #6044, #4483, #6676, .T. ) ;
#7915=VECTOR ( 'NONE', #2869, 1000.000000000000000 ) ;
#7942=COLOUR_RGB('Light Blue',0.38,0.62,0.78);
#7943=FILL_AREA_STYLE_COLOUR('',#7942);
#7944=FILL_AREA_STYLE('',(#7943));
#7945=SURFACE_STYLE_FILL_AREA(#7944);
#7946=SURFACE_SIDE_STYLE('',(#7945));
#7947=SURFACE_STYLE_USAGE(.BOTH.,#7946);
#7948=PRESENTATION_STYLE_ASSIGNMENT((#7947));
ENDSEC;
END-ISO-10303-21;
